ISO-10303-21;
HEADER;
/* Generated by software containing ST-Developer
 * from STEP Tools, Inc. (www.steptools.com) 
 */

FILE_DESCRIPTION(
/* description */ ('PAT-091'),
/* implementation_level */ '2;1');

FILE_NAME(
/* name */ 'M4 low-profile retaining screw (15).step',
/* time_stamp */ '2026-10-27T15:34:44-07:00',
/* author */ (''),
/* organization */ (''),
/* preprocessor_version */ 'ST-DEVELOPER v20.2',
/* originating_system */ 'Autodesk Translation Framework v15.17.0.0',
/* authorisation */ '');

FILE_SCHEMA (('AUTOMOTIVE_DESIGN { 1 0 10303 214 3 1 1 }'));
ENDSEC;

DATA;
#10=MECHANICAL_DESIGN_GEOMETRIC_PRESENTATION_REPRESENTATION('',(#1069),#25100);
#849=SHAPE_REPRESENTATION_RELATIONSHIP('SRR','None',#25616,#959);
#959=ADVANCED_BREP_SHAPE_REPRESENTATION('',(#1190),#25086);
#1069=STYLED_ITEM('',(#26198),#1190);
#1190=MANIFOLD_SOLID_BREP('Body1',#13349);
#1616=FACE_BOUND('',#3990,.T.);
#2021=PLANE('',#16123);
#2022=PLANE('',#16128);
#2023=PLANE('',#16131);
#2770=FACE_OUTER_BOUND('',#3989,.T.);
#2771=FACE_OUTER_BOUND('',#3991,.T.);
#2772=FACE_OUTER_BOUND('',#3992,.T.);
#2773=FACE_OUTER_BOUND('',#3993,.T.);
#2774=FACE_OUTER_BOUND('',#3994,.T.);
#3989=EDGE_LOOP('',(#11696));
#3990=EDGE_LOOP('',(#11697));
#3991=EDGE_LOOP('',(#11698,#11699,#11700,#11701));
#3992=EDGE_LOOP('',(#11702));
#3993=EDGE_LOOP('',(#11703,#11704,#11705,#11706));
#3994=EDGE_LOOP('',(#11707));
#4832=LINE('',#24188,#5572);
#4833=LINE('',#24192,#5573);
#5572=VECTOR('',#20262,0.350000000000001);
#5573=VECTOR('',#20267,0.199999999999999);
#6254=CIRCLE('',#16124,0.350000000000001);
#6255=CIRCLE('',#16125,0.199999999999999);
#6256=CIRCLE('',#16127,0.350000000000001);
#6257=CIRCLE('',#16130,0.199999999999999);
#7287=VERTEX_POINT('',#24181);
#7288=VERTEX_POINT('',#24183);
#7289=VERTEX_POINT('',#24186);
#7290=VERTEX_POINT('',#24191);
#8783=EDGE_CURVE('',#7287,#7287,#6254,.T.);
#8784=EDGE_CURVE('',#7288,#7288,#6255,.T.);
#8785=EDGE_CURVE('',#7289,#7289,#6256,.T.);
#8786=EDGE_CURVE('',#7289,#7287,#4832,.T.);
#8787=EDGE_CURVE('',#7288,#7290,#4833,.T.);
#8788=EDGE_CURVE('',#7290,#7290,#6257,.T.);
#11696=ORIENTED_EDGE('',*,*,#8783,.F.);
#11697=ORIENTED_EDGE('',*,*,#8784,.T.);
#11698=ORIENTED_EDGE('',*,*,#8785,.F.);
#11699=ORIENTED_EDGE('',*,*,#8786,.T.);
#11700=ORIENTED_EDGE('',*,*,#8783,.T.);
#11701=ORIENTED_EDGE('',*,*,#8786,.F.);
#11702=ORIENTED_EDGE('',*,*,#8785,.T.);
#11703=ORIENTED_EDGE('',*,*,#8784,.F.);
#11704=ORIENTED_EDGE('',*,*,#8787,.T.);
#11705=ORIENTED_EDGE('',*,*,#8788,.T.);
#11706=ORIENTED_EDGE('',*,*,#8787,.F.);
#11707=ORIENTED_EDGE('',*,*,#8788,.F.);
#12388=CYLINDRICAL_SURFACE('',#16126,0.350000000000001);
#12389=CYLINDRICAL_SURFACE('',#16129,0.199999999999999);
#13137=ADVANCED_FACE('',(#2770,#1616),#2021,.F.);
#13138=ADVANCED_FACE('',(#2771),#12388,.T.);
#13139=ADVANCED_FACE('',(#2772),#2022,.T.);
#13140=ADVANCED_FACE('',(#2773),#12389,.T.);
#13141=ADVANCED_FACE('',(#2774),#2023,.F.);
#13349=CLOSED_SHELL('',(#13137,#13138,#13139,#13140,#13141));
#16122=AXIS2_PLACEMENT_3D('',#24179,#20250,#20251);
#16123=AXIS2_PLACEMENT_3D('',#24180,#20252,#20253);
#16124=AXIS2_PLACEMENT_3D('',#24182,#20254,#20255);
#16125=AXIS2_PLACEMENT_3D('',#24184,#20256,#20257);
#16126=AXIS2_PLACEMENT_3D('',#24185,#20258,#20259);
#16127=AXIS2_PLACEMENT_3D('',#24187,#20260,#20261);
#16128=AXIS2_PLACEMENT_3D('',#24189,#20263,#20264);
#16129=AXIS2_PLACEMENT_3D('',#24190,#20265,#20266);
#16130=AXIS2_PLACEMENT_3D('',#24193,#20268,#20269);
#16131=AXIS2_PLACEMENT_3D('',#24194,#20270,#20271);
#20250=DIRECTION('axis',(0.,0.,1.));
#20251=DIRECTION('refdir',(1.,0.,0.));
#20252=DIRECTION('center_axis',(0.,1.,0.));
#20253=DIRECTION('ref_axis',(1.,0.,0.));
#20254=DIRECTION('center_axis',(0.,1.,0.));
#20255=DIRECTION('ref_axis',(1.,0.,0.));
#20256=DIRECTION('center_axis',(0.,1.,0.));
#20257=DIRECTION('ref_axis',(1.,0.,0.));
#20258=DIRECTION('center_axis',(0.,1.,0.));
#20259=DIRECTION('ref_axis',(1.,0.,0.));
#20260=DIRECTION('center_axis',(0.,1.,0.));
#20261=DIRECTION('ref_axis',(1.,0.,0.));
#20262=DIRECTION('',(0.,-1.,0.));
#20263=DIRECTION('center_axis',(0.,1.,0.));
#20264=DIRECTION('ref_axis',(1.,0.,0.));
#20265=DIRECTION('center_axis',(0.,1.,0.));
#20266=DIRECTION('ref_axis',(1.,0.,0.));
#20267=DIRECTION('',(0.,-1.,0.));
#20268=DIRECTION('center_axis',(0.,1.,0.));
#20269=DIRECTION('ref_axis',(1.,0.,0.));
#20270=DIRECTION('center_axis',(0.,1.,0.));
#20271=DIRECTION('ref_axis',(1.,0.,0.));
#24179=CARTESIAN_POINT('',(0.,0.,0.));
#24180=CARTESIAN_POINT('Origin',(20.6730642762322,8.3,6.69185245480489));
#24181=CARTESIAN_POINT('',(20.3230642762322,8.3,6.69185245480489));
#24182=CARTESIAN_POINT('Origin',(20.6730642762322,8.3,6.69185245480489));
#24183=CARTESIAN_POINT('',(20.4730642762322,8.3,6.69185245480489));
#24184=CARTESIAN_POINT('Origin',(20.6730642762322,8.3,6.69185245480489));
#24185=CARTESIAN_POINT('Origin',(20.6730642762322,8.3,6.69185245480489));
#24186=CARTESIAN_POINT('',(20.3230642762322,8.4,6.69185245480489));
#24187=CARTESIAN_POINT('Origin',(20.6730642762322,8.4,6.69185245480489));
#24188=CARTESIAN_POINT('',(20.3230642762322,8.3,6.69185245480489));
#24189=CARTESIAN_POINT('Origin',(20.6730642762322,8.4,6.69185245480489));
#24190=CARTESIAN_POINT('Origin',(20.6730642762322,7.6,6.69185245480489));
#24191=CARTESIAN_POINT('',(20.4730642762322,7.6,6.69185245480489));
#24192=CARTESIAN_POINT('',(20.4730642762322,7.6,6.69185245480489));
#24193=CARTESIAN_POINT('Origin',(20.6730642762322,7.6,6.69185245480489));
#24194=CARTESIAN_POINT('Origin',(20.6730642762322,7.6,6.69185245480489));
#24965=UNCERTAINTY_MEASURE_WITH_UNIT(LENGTH_MEASURE(0.001),#25101,
'DISTANCE_ACCURACY_VALUE',
'Maximum model space distance between geometric entities at asserted c
onnectivities');
#24979=UNCERTAINTY_MEASURE_WITH_UNIT(LENGTH_MEASURE(0.001),#25101,
'DISTANCE_ACCURACY_VALUE',
'Maximum model space distance between geometric entities at asserted c
onnectivities');
#25086=(
GEOMETRIC_REPRESENTATION_CONTEXT(3)
GLOBAL_UNCERTAINTY_ASSIGNED_CONTEXT((#24965))
GLOBAL_UNIT_ASSIGNED_CONTEXT((#25101,#25103,#25104))
REPRESENTATION_CONTEXT('','3D')
);
#25100=(
GEOMETRIC_REPRESENTATION_CONTEXT(3)
GLOBAL_UNCERTAINTY_ASSIGNED_CONTEXT((#24979))
GLOBAL_UNIT_ASSIGNED_CONTEXT((#25101,#25103,#25104))
REPRESENTATION_CONTEXT('','3D')
);
#25101=(
LENGTH_UNIT()
NAMED_UNIT(*)
SI_UNIT(.CENTI.,.METRE.)
);
#25103=(
NAMED_UNIT(*)
PLANE_ANGLE_UNIT()
SI_UNIT($,.RADIAN.)
);
#25104=(
NAMED_UNIT(*)
SI_UNIT($,.STERADIAN.)
SOLID_ANGLE_UNIT()
);
#25211=SHAPE_DEFINITION_REPRESENTATION(#25405,#25616);
#25405=PRODUCT_DEFINITION_SHAPE('',$,#25737);
#25616=SHAPE_REPRESENTATION('',(#16122),#25086);
#25630=PRODUCT_DEFINITION_CONTEXT('part definition',#25992,'design');
#25737=PRODUCT_DEFINITION('M4 low-profile retaining screw (15)',
'M4 low-profile retaining screw (15)',#25857,#25630);
#25857=PRODUCT_DEFINITION_FORMATION('',$,#26100);
#25992=APPLICATION_CONTEXT(
'Core Data for Automotive Mechanical Design Process');
#25993=PRODUCT_CONTEXT('part definition',#25992,'mechanical');
#26100=PRODUCT('M4 low-profile retaining screw (15)',
'M4 low-profile retaining screw (15)','M4 low-profile retaining screw (15)',
(#25993));
#26192=COLOUR_RGB('Black',0.12,0.14,0.17);
#26193=FILL_AREA_STYLE_COLOUR('',#26192);
#26194=FILL_AREA_STYLE('',(#26193));
#26195=SURFACE_STYLE_FILL_AREA(#26194);
#26196=SURFACE_SIDE_STYLE('',(#26195));
#26197=SURFACE_STYLE_USAGE(.BOTH.,#26196);
#26198=PRESENTATION_STYLE_ASSIGNMENT((#26197));
ENDSEC;
END-ISO-10303-21;
